ISO-10303-21;
HEADER;
/* Generated by software containing ST-Developer
 * from STEP Tools, Inc. (www.steptools.com) 
 */

FILE_DESCRIPTION(
/* description */ ('Rack and pinion manual slide'),
/* implementation_level */ '2;1');

FILE_NAME(
/* name */ 'Cap Screw - M6x25.step',
/* time_stamp */ '2026-10-28T03:22:49-07:00',
/* author */ (''),
/* organization */ (''),
/* preprocessor_version */ 'ST-DEVELOPER v20.2',
/* originating_system */ 'Autodesk Translation Framework v15.17.0.0',
/* authorisation */ '');

FILE_SCHEMA (('AUTOMOTIVE_DESIGN { 1 0 10303 214 3 1 1 }'));
ENDSEC;

DATA;
#10=MECHANICAL_DESIGN_GEOMETRIC_PRESENTATION_REPRESENTATION('',(#783),#34851);
#609=ORIENTED_CLOSED_SHELL('',*,#13808,.F.);
#614=BREP_WITH_VOIDS('Body1',#13807,(#609));
#634=CONICAL_SURFACE('',#15546,0.475,0.785398163397449);
#635=CONICAL_SURFACE('',#15550,0.485,0.785398163397448);
#636=CONICAL_SURFACE('',#15554,0.31,0.463647609000806);
#637=CONICAL_SURFACE('',#15558,0.27,0.785398163397448);
#684=SHAPE_REPRESENTATION_RELATIONSHIP('SRR','None',#35123,#730);
#730=ADVANCED_BREP_SHAPE_REPRESENTATION('',(#614),#34848);
#783=STYLED_ITEM('',(#35418),#614);
#1041=FACE_BOUND('',#3205,.T.);
#1522=PLANE('',#15544);
#1523=PLANE('',#15552);
#1524=PLANE('',#15560);
#1525=PLANE('',#15561);
#1526=PLANE('',#15562);
#1527=PLANE('',#15563);
#1528=PLANE('',#15564);
#1529=PLANE('',#15565);
#1530=PLANE('',#15566);
#1531=PLANE('',#15567);
#1532=PLANE('',#15568);
#2253=FACE_OUTER_BOUND('',#3200,.T.);
#2254=FACE_OUTER_BOUND('',#3201,.T.);
#2255=FACE_OUTER_BOUND('',#3202,.T.);
#2256=FACE_OUTER_BOUND('',#3203,.T.);
#2257=FACE_OUTER_BOUND('',#3204,.T.);
#2258=FACE_OUTER_BOUND('',#3206,.T.);
#2259=FACE_OUTER_BOUND('',#3207,.T.);
#2260=FACE_OUTER_BOUND('',#3208,.T.);
#2261=FACE_OUTER_BOUND('',#3209,.T.);
#2262=FACE_OUTER_BOUND('',#3210,.T.);
#2263=FACE_OUTER_BOUND('',#3211,.T.);
#2264=FACE_OUTER_BOUND('',#3212,.T.);
#2265=FACE_OUTER_BOUND('',#3213,.T.);
#2266=FACE_OUTER_BOUND('',#3214,.T.);
#2267=FACE_OUTER_BOUND('',#3215,.T.);
#2268=FACE_OUTER_BOUND('',#3216,.T.);
#2269=FACE_OUTER_BOUND('',#3217,.T.);
#3200=EDGE_LOOP('',(#12768));
#3201=EDGE_LOOP('',(#12769,#12770,#12771,#12772));
#3202=EDGE_LOOP('',(#12773,#12774,#12775,#12776));
#3203=EDGE_LOOP('',(#12777,#12778,#12779,#12780));
#3204=EDGE_LOOP('',(#12781));
#3205=EDGE_LOOP('',(#12782));
#3206=EDGE_LOOP('',(#12783,#12784,#12785,#12786));
#3207=EDGE_LOOP('',(#12787,#12788,#12789,#12790));
#3208=EDGE_LOOP('',(#12791,#12792,#12793,#12794));
#3209=EDGE_LOOP('',(#12795));
#3210=EDGE_LOOP('',(#12796,#12797,#12798,#12799));
#3211=EDGE_LOOP('',(#12800,#12801,#12802,#12803));
#3212=EDGE_LOOP('',(#12804,#12805,#12806,#12807));
#3213=EDGE_LOOP('',(#12808,#12809,#12810,#12811));
#3214=EDGE_LOOP('',(#12812,#12813,#12814,#12815));
#3215=EDGE_LOOP('',(#12816,#12817,#12818,#12819));
#3216=EDGE_LOOP('',(#12820,#12821,#12822,#12823,#12824,#12825));
#3217=EDGE_LOOP('',(#12826,#12827,#12828,#12829,#12830,#12831));
#4489=LINE('',#34644,#5780);
#4490=LINE('',#34648,#5781);
#4491=LINE('',#34652,#5782);
#4492=LINE('',#34659,#5783);
#4493=LINE('',#34663,#5784);
#4494=LINE('',#34667,#5785);
#4495=LINE('',#34672,#5786);
#4496=LINE('',#34674,#5787);
#4497=LINE('',#34676,#5788);
#4498=LINE('',#34677,#5789);
#4499=LINE('',#34680,#5790);
#4500=LINE('',#34682,#5791);
#4501=LINE('',#34683,#5792);
#4502=LINE('',#34686,#5793);
#4503=LINE('',#34688,#5794);
#4504=LINE('',#34689,#5795);
#4505=LINE('',#34692,#5796);
#4506=LINE('',#34694,#5797);
#4507=LINE('',#34695,#5798);
#4508=LINE('',#34698,#5799);
#4509=LINE('',#34700,#5800);
#4510=LINE('',#34701,#5801);
#4511=LINE('',#34703,#5802);
#4512=LINE('',#34704,#5803);
#5780=VECTOR('',#19327,0.475);
#5781=VECTOR('',#19332,0.5);
#5782=VECTOR('',#19337,0.485);
#5783=VECTOR('',#19346,0.31);
#5784=VECTOR('',#19351,0.3);
#5785=VECTOR('',#19356,0.27);
#5786=VECTOR('',#19361,1.);
#5787=VECTOR('',#19362,1.);
#5788=VECTOR('',#19363,1.);
#5789=VECTOR('',#19364,1.);
#5790=VECTOR('',#19367,1.);
#5791=VECTOR('',#19368,1.);
#5792=VECTOR('',#19369,1.);
#5793=VECTOR('',#19372,1.);
#5794=VECTOR('',#19373,1.);
#5795=VECTOR('',#19374,1.);
#5796=VECTOR('',#19377,1.);
#5797=VECTOR('',#19378,1.);
#5798=VECTOR('',#19379,1.);
#5799=VECTOR('',#19382,1.);
#5800=VECTOR('',#19383,1.);
#5801=VECTOR('',#19384,1.);
#5802=VECTOR('',#19387,1.);
#5803=VECTOR('',#19388,1.);
#6212=CIRCLE('',#15545,0.45);
#6213=CIRCLE('',#15547,0.5);
#6214=CIRCLE('',#15549,0.5);
#6215=CIRCLE('',#15551,0.47);
#6216=CIRCLE('',#15553,0.32);
#6217=CIRCLE('',#15555,0.2942);
#6218=CIRCLE('',#15557,0.2942);
#6219=CIRCLE('',#15559,0.24);
#7405=VERTEX_POINT('',#34639);
#7406=VERTEX_POINT('',#34642);
#7407=VERTEX_POINT('',#34646);
#7408=VERTEX_POINT('',#34650);
#7409=VERTEX_POINT('',#34654);
#7410=VERTEX_POINT('',#34657);
#7411=VERTEX_POINT('',#34661);
#7412=VERTEX_POINT('',#34665);
#7413=VERTEX_POINT('',#34670);
#7414=VERTEX_POINT('',#34671);
#7415=VERTEX_POINT('',#34673);
#7416=VERTEX_POINT('',#34675);
#7417=VERTEX_POINT('',#34679);
#7418=VERTEX_POINT('',#34681);
#7419=VERTEX_POINT('',#34685);
#7420=VERTEX_POINT('',#34687);
#7421=VERTEX_POINT('',#34691);
#7422=VERTEX_POINT('',#34693);
#7423=VERTEX_POINT('',#34697);
#7424=VERTEX_POINT('',#34699);
#9196=EDGE_CURVE('',#7405,#7405,#6212,.T.);
#9197=EDGE_CURVE('',#7406,#7406,#6213,.T.);
#9198=EDGE_CURVE('',#7406,#7405,#4489,.T.);
#9199=EDGE_CURVE('',#7407,#7407,#6214,.T.);
#9200=EDGE_CURVE('',#7407,#7406,#4490,.T.);
#9201=EDGE_CURVE('',#7408,#7408,#6215,.T.);
#9202=EDGE_CURVE('',#7408,#7407,#4491,.T.);
#9203=EDGE_CURVE('',#7409,#7409,#6216,.T.);
#9204=EDGE_CURVE('',#7410,#7410,#6217,.F.);
#9205=EDGE_CURVE('',#7410,#7409,#4492,.T.);
#9206=EDGE_CURVE('',#7411,#7411,#6218,.F.);
#9207=EDGE_CURVE('',#7411,#7410,#4493,.T.);
#9208=EDGE_CURVE('',#7412,#7412,#6219,.T.);
#9209=EDGE_CURVE('',#7412,#7411,#4494,.T.);
#9210=EDGE_CURVE('',#7413,#7414,#4495,.T.);
#9211=EDGE_CURVE('',#7414,#7415,#4496,.T.);
#9212=EDGE_CURVE('',#7415,#7416,#4497,.T.);
#9213=EDGE_CURVE('',#7413,#7416,#4498,.T.);
#9214=EDGE_CURVE('',#7414,#7417,#4499,.T.);
#9215=EDGE_CURVE('',#7417,#7418,#4500,.T.);
#9216=EDGE_CURVE('',#7418,#7415,#4501,.T.);
#9217=EDGE_CURVE('',#7417,#7419,#4502,.T.);
#9218=EDGE_CURVE('',#7419,#7420,#4503,.T.);
#9219=EDGE_CURVE('',#7420,#7418,#4504,.T.);
#9220=EDGE_CURVE('',#7419,#7421,#4505,.T.);
#9221=EDGE_CURVE('',#7421,#7422,#4506,.T.);
#9222=EDGE_CURVE('',#7422,#7420,#4507,.T.);
#9223=EDGE_CURVE('',#7421,#7423,#4508,.T.);
#9224=EDGE_CURVE('',#7423,#7424,#4509,.T.);
#9225=EDGE_CURVE('',#7424,#7422,#4510,.T.);
#9226=EDGE_CURVE('',#7423,#7413,#4511,.T.);
#9227=EDGE_CURVE('',#7416,#7424,#4512,.T.);
#12768=ORIENTED_EDGE('',*,*,#9196,.F.);
#12769=ORIENTED_EDGE('',*,*,#9197,.F.);
#12770=ORIENTED_EDGE('',*,*,#9198,.T.);
#12771=ORIENTED_EDGE('',*,*,#9196,.T.);
#12772=ORIENTED_EDGE('',*,*,#9198,.F.);
#12773=ORIENTED_EDGE('',*,*,#9199,.F.);
#12774=ORIENTED_EDGE('',*,*,#9200,.T.);
#12775=ORIENTED_EDGE('',*,*,#9197,.T.);
#12776=ORIENTED_EDGE('',*,*,#9200,.F.);
#12777=ORIENTED_EDGE('',*,*,#9201,.F.);
#12778=ORIENTED_EDGE('',*,*,#9202,.T.);
#12779=ORIENTED_EDGE('',*,*,#9199,.T.);
#12780=ORIENTED_EDGE('',*,*,#9202,.F.);
#12781=ORIENTED_EDGE('',*,*,#9201,.T.);
#12782=ORIENTED_EDGE('',*,*,#9203,.F.);
#12783=ORIENTED_EDGE('',*,*,#9204,.F.);
#12784=ORIENTED_EDGE('',*,*,#9205,.T.);
#12785=ORIENTED_EDGE('',*,*,#9203,.T.);
#12786=ORIENTED_EDGE('',*,*,#9205,.F.);
#12787=ORIENTED_EDGE('',*,*,#9206,.F.);
#12788=ORIENTED_EDGE('',*,*,#9207,.T.);
#12789=ORIENTED_EDGE('',*,*,#9204,.T.);
#12790=ORIENTED_EDGE('',*,*,#9207,.F.);
#12791=ORIENTED_EDGE('',*,*,#9208,.F.);
#12792=ORIENTED_EDGE('',*,*,#9209,.T.);
#12793=ORIENTED_EDGE('',*,*,#9206,.T.);
#12794=ORIENTED_EDGE('',*,*,#9209,.F.);
#12795=ORIENTED_EDGE('',*,*,#9208,.T.);
#12796=ORIENTED_EDGE('',*,*,#9210,.T.);
#12797=ORIENTED_EDGE('',*,*,#9211,.T.);
#12798=ORIENTED_EDGE('',*,*,#9212,.T.);
#12799=ORIENTED_EDGE('',*,*,#9213,.F.);
#12800=ORIENTED_EDGE('',*,*,#9214,.T.);
#12801=ORIENTED_EDGE('',*,*,#9215,.T.);
#12802=ORIENTED_EDGE('',*,*,#9216,.T.);
#12803=ORIENTED_EDGE('',*,*,#9211,.F.);
#12804=ORIENTED_EDGE('',*,*,#9217,.T.);
#12805=ORIENTED_EDGE('',*,*,#9218,.T.);
#12806=ORIENTED_EDGE('',*,*,#9219,.T.);
#12807=ORIENTED_EDGE('',*,*,#9215,.F.);
#12808=ORIENTED_EDGE('',*,*,#9220,.T.);
#12809=ORIENTED_EDGE('',*,*,#9221,.T.);
#12810=ORIENTED_EDGE('',*,*,#9222,.T.);
#12811=ORIENTED_EDGE('',*,*,#9218,.F.);
#12812=ORIENTED_EDGE('',*,*,#9223,.T.);
#12813=ORIENTED_EDGE('',*,*,#9224,.T.);
#12814=ORIENTED_EDGE('',*,*,#9225,.T.);
#12815=ORIENTED_EDGE('',*,*,#9221,.F.);
#12816=ORIENTED_EDGE('',*,*,#9226,.T.);
#12817=ORIENTED_EDGE('',*,*,#9213,.T.);
#12818=ORIENTED_EDGE('',*,*,#9227,.T.);
#12819=ORIENTED_EDGE('',*,*,#9224,.F.);
#12820=ORIENTED_EDGE('',*,*,#9226,.F.);
#12821=ORIENTED_EDGE('',*,*,#9223,.F.);
#12822=ORIENTED_EDGE('',*,*,#9220,.F.);
#12823=ORIENTED_EDGE('',*,*,#9217,.F.);
#12824=ORIENTED_EDGE('',*,*,#9214,.F.);
#12825=ORIENTED_EDGE('',*,*,#9210,.F.);
#12826=ORIENTED_EDGE('',*,*,#9227,.F.);
#12827=ORIENTED_EDGE('',*,*,#9212,.F.);
#12828=ORIENTED_EDGE('',*,*,#9216,.F.);
#12829=ORIENTED_EDGE('',*,*,#9219,.F.);
#12830=ORIENTED_EDGE('',*,*,#9222,.F.);
#12831=ORIENTED_EDGE('',*,*,#9225,.F.);
#13009=CYLINDRICAL_SURFACE('',#15548,0.5);
#13010=CYLINDRICAL_SURFACE('',#15556,0.2942);
#13731=ADVANCED_FACE('',(#2253),#1522,.T.);
#13732=ADVANCED_FACE('',(#2254),#634,.T.);
#13733=ADVANCED_FACE('',(#2255),#13009,.T.);
#13734=ADVANCED_FACE('',(#2256),#635,.T.);
#13735=ADVANCED_FACE('',(#2257,#1041),#1523,.T.);
#13736=ADVANCED_FACE('',(#2258),#636,.T.);
#13737=ADVANCED_FACE('',(#2259),#13010,.T.);
#13738=ADVANCED_FACE('',(#2260),#637,.T.);
#13739=ADVANCED_FACE('',(#2261),#1524,.T.);
#13740=ADVANCED_FACE('',(#2262),#1525,.F.);
#13741=ADVANCED_FACE('',(#2263),#1526,.F.);
#13742=ADVANCED_FACE('',(#2264),#1527,.F.);
#13743=ADVANCED_FACE('',(#2265),#1528,.F.);
#13744=ADVANCED_FACE('',(#2266),#1529,.F.);
#13745=ADVANCED_FACE('',(#2267),#1530,.F.);
#13746=ADVANCED_FACE('',(#2268),#1531,.F.);
#13747=ADVANCED_FACE('',(#2269),#1532,.F.);
#13807=CLOSED_SHELL('',(#13731,#13732,#13733,#13734,#13735,#13736,#13737,
#13738,#13739));
#13808=CLOSED_SHELL('',(#13740,#13741,#13742,#13743,#13744,#13745,#13746,
#13747));
#15543=AXIS2_PLACEMENT_3D('',#34637,#19317,#19318);
#15544=AXIS2_PLACEMENT_3D('',#34638,#19319,#19320);
#15545=AXIS2_PLACEMENT_3D('',#34640,#19321,#19322);
#15546=AXIS2_PLACEMENT_3D('',#34641,#19323,#19324);
#15547=AXIS2_PLACEMENT_3D('',#34643,#19325,#19326);
#15548=AXIS2_PLACEMENT_3D('',#34645,#19328,#19329);
#15549=AXIS2_PLACEMENT_3D('',#34647,#19330,#19331);
#15550=AXIS2_PLACEMENT_3D('',#34649,#19333,#19334);
#15551=AXIS2_PLACEMENT_3D('',#34651,#19335,#19336);
#15552=AXIS2_PLACEMENT_3D('',#34653,#19338,#19339);
#15553=AXIS2_PLACEMENT_3D('',#34655,#19340,#19341);
#15554=AXIS2_PLACEMENT_3D('',#34656,#19342,#19343);
#15555=AXIS2_PLACEMENT_3D('',#34658,#19344,#19345);
#15556=AXIS2_PLACEMENT_3D('',#34660,#19347,#19348);
#15557=AXIS2_PLACEMENT_3D('',#34662,#19349,#19350);
#15558=AXIS2_PLACEMENT_3D('',#34664,#19352,#19353);
#15559=AXIS2_PLACEMENT_3D('',#34666,#19354,#19355);
#15560=AXIS2_PLACEMENT_3D('',#34668,#19357,#19358);
#15561=AXIS2_PLACEMENT_3D('',#34669,#19359,#19360);
#15562=AXIS2_PLACEMENT_3D('',#34678,#19365,#19366);
#15563=AXIS2_PLACEMENT_3D('',#34684,#19370,#19371);
#15564=AXIS2_PLACEMENT_3D('',#34690,#19375,#19376);
#15565=AXIS2_PLACEMENT_3D('',#34696,#19380,#19381);
#15566=AXIS2_PLACEMENT_3D('',#34702,#19385,#19386);
#15567=AXIS2_PLACEMENT_3D('',#34705,#19389,#19390);
#15568=AXIS2_PLACEMENT_3D('',#34706,#19391,#19392);
#19317=DIRECTION('axis',(0.,0.,1.));
#19318=DIRECTION('refdir',(1.,0.,0.));
#19319=DIRECTION('center_axis',(0.,1.,0.));
#19320=DIRECTION('ref_axis',(0.,0.,1.));
#19321=DIRECTION('center_axis',(0.,-1.,0.));
#19322=DIRECTION('ref_axis',(1.,0.,0.));
#19323=DIRECTION('center_axis',(0.,-1.,0.));
#19324=DIRECTION('ref_axis',(1.,0.,0.));
#19325=DIRECTION('center_axis',(0.,-1.,0.));
#19326=DIRECTION('ref_axis',(1.,0.,0.));
#19327=DIRECTION('',(0.707106781186548,0.707106781186547,8.65956056235494E-17));
#19328=DIRECTION('center_axis',(0.,-1.,0.));
#19329=DIRECTION('ref_axis',(1.,0.,0.));
#19330=DIRECTION('center_axis',(0.,-1.,0.));
#19331=DIRECTION('ref_axis',(1.,0.,0.));
#19332=DIRECTION('',(0.,1.,0.));
#19333=DIRECTION('center_axis',(0.,1.,0.));
#19334=DIRECTION('ref_axis',(1.,0.,0.));
#19335=DIRECTION('center_axis',(0.,-1.,0.));
#19336=DIRECTION('ref_axis',(1.,0.,0.));
#19337=DIRECTION('',(-0.707106781186547,0.707106781186548,-8.65956056235493E-17));
#19338=DIRECTION('center_axis',(0.,-1.,0.));
#19339=DIRECTION('ref_axis',(0.,0.,-1.));
#19340=DIRECTION('center_axis',(0.,-1.,0.));
#19341=DIRECTION('ref_axis',(1.,0.,0.));
#19342=DIRECTION('center_axis',(0.,1.,0.));
#19343=DIRECTION('ref_axis',(1.,0.,0.));
#19344=DIRECTION('center_axis',(0.,1.,0.));
#19345=DIRECTION('ref_axis',(1.,0.,0.));
#19346=DIRECTION('',(-0.447213595499958,0.894427190999916,-5.47678698264203E-17));
#19347=DIRECTION('center_axis',(0.,-1.,0.));
#19348=DIRECTION('ref_axis',(1.,0.,0.));
#19349=DIRECTION('center_axis',(0.,1.,0.));
#19350=DIRECTION('ref_axis',(1.,0.,0.));
#19351=DIRECTION('',(0.,1.,0.));
#19352=DIRECTION('center_axis',(0.,1.,0.));
#19353=DIRECTION('ref_axis',(1.,0.,0.));
#19354=DIRECTION('center_axis',(0.,-1.,0.));
#19355=DIRECTION('ref_axis',(1.,0.,0.));
#19356=DIRECTION('',(-0.707106781186547,0.707106781186548,-8.65956056235493E-17));
#19357=DIRECTION('center_axis',(0.,-1.,0.));
#19358=DIRECTION('ref_axis',(0.,0.,-1.));
#19359=DIRECTION('center_axis',(0.866025403784439,0.,-0.5));
#19360=DIRECTION('ref_axis',(0.5,0.,0.866025403784439));
#19361=DIRECTION('',(-0.5,0.,-0.866025403784439));
#19362=DIRECTION('',(0.,-1.,0.));
#19363=DIRECTION('',(0.5,0.,0.866025403784439));
#19364=DIRECTION('',(0.,-1.,0.));
#19365=DIRECTION('center_axis',(1.92296268638356E-16,0.,-1.));
#19366=DIRECTION('ref_axis',(1.,0.,1.92296268638356E-16));
#19367=DIRECTION('',(-1.,0.,-1.92296268638356E-16));
#19368=DIRECTION('',(0.,-1.,0.));
#19369=DIRECTION('',(1.,0.,1.92296268638356E-16));
#19370=DIRECTION('center_axis',(-0.866025403784439,0.,-0.5));
#19371=DIRECTION('ref_axis',(0.5,0.,-0.866025403784439));
#19372=DIRECTION('',(-0.5,0.,0.866025403784438));
#19373=DIRECTION('',(0.,-1.,0.));
#19374=DIRECTION('',(0.5,0.,-0.866025403784438));
#19375=DIRECTION('center_axis',(-0.866025403784439,0.,0.5));
#19376=DIRECTION('ref_axis',(-0.5,0.,-0.866025403784439));
#19377=DIRECTION('',(0.5,0.,0.866025403784439));
#19378=DIRECTION('',(0.,-1.,0.));
#19379=DIRECTION('',(-0.5,0.,-0.866025403784439));
#19380=DIRECTION('center_axis',(-1.92296268638356E-16,0.,1.));
#19381=DIRECTION('ref_axis',(-1.,0.,-1.92296268638356E-16));
#19382=DIRECTION('',(1.,0.,1.92296268638356E-16));
#19383=DIRECTION('',(0.,-1.,0.));
#19384=DIRECTION('',(-1.,0.,-1.92296268638356E-16));
#19385=DIRECTION('center_axis',(0.866025403784439,0.,0.5));
#19386=DIRECTION('ref_axis',(-0.5,0.,0.866025403784439));
#19387=DIRECTION('',(0.5,0.,-0.866025403784439));
#19388=DIRECTION('',(-0.5,0.,0.866025403784439));
#19389=DIRECTION('center_axis',(0.,1.,0.));
#19390=DIRECTION('ref_axis',(1.,0.,0.));
#19391=DIRECTION('center_axis',(0.,-1.,0.));
#19392=DIRECTION('ref_axis',(0.,0.,-1.));
#34637=CARTESIAN_POINT('',(0.,0.,0.));
#34638=CARTESIAN_POINT('Origin',(0.45,0.6,0.));
#34639=CARTESIAN_POINT('',(-0.45,0.6,-5.51091059616309E-17));
#34640=CARTESIAN_POINT('Origin',(0.,0.6,0.));
#34641=CARTESIAN_POINT('Origin',(0.,0.575,0.));
#34642=CARTESIAN_POINT('',(-0.5,0.55,-6.12323399573677E-17));
#34643=CARTESIAN_POINT('Origin',(0.,0.55,0.));
#34644=CARTESIAN_POINT('',(-0.475,0.575,-5.81707229594993E-17));
#34645=CARTESIAN_POINT('Origin',(0.,0.29,0.));
#34646=CARTESIAN_POINT('',(-0.5,0.0299999999999998,-6.12323399573677E-17));
#34647=CARTESIAN_POINT('Origin',(0.,0.0299999999999998,0.));
#34648=CARTESIAN_POINT('',(-0.5,0.29,-6.12323399573677E-17));
#34649=CARTESIAN_POINT('Origin',(0.,0.0150000000000001,0.));
#34650=CARTESIAN_POINT('',(-0.47,7.11236625150491E-17,-5.75583995599256E-17));
#34651=CARTESIAN_POINT('Origin',(0.,0.,0.));
#34652=CARTESIAN_POINT('',(-0.485,0.0150000000000001,-5.93953697586466E-17));
#34653=CARTESIAN_POINT('Origin',(0.32,0.,0.));
#34654=CARTESIAN_POINT('',(-0.32,-6.93889390390723E-18,-3.91886975727153E-17));
#34655=CARTESIAN_POINT('Origin',(0.,0.,0.));
#34656=CARTESIAN_POINT('Origin',(0.,-0.02,0.));
#34657=CARTESIAN_POINT('',(-0.2942,-0.0515999999999999,3.60291088309151E-17));
#34658=CARTESIAN_POINT('Origin',(0.,-0.0515999999999999,0.));
#34659=CARTESIAN_POINT('',(-0.31,-0.02,-3.7964050773568E-17));
#34660=CARTESIAN_POINT('Origin',(0.,-1.24,0.));
#34661=CARTESIAN_POINT('',(-0.2942,-2.4458,3.60291088309151E-17));
#34662=CARTESIAN_POINT('Origin',(0.,-2.4458,0.));
#34663=CARTESIAN_POINT('',(-0.2942,-1.24,-3.60291088309151E-17));
#34664=CARTESIAN_POINT('Origin',(0.,-2.47,0.));
#34665=CARTESIAN_POINT('',(-0.24,-2.5,-2.93915231795365E-17));
#34666=CARTESIAN_POINT('Origin',(0.,-2.5,0.));
#34667=CARTESIAN_POINT('',(-0.27,-2.47,-3.30654635769785E-17));
#34668=CARTESIAN_POINT('Origin',(0.,-2.5,0.));
#34669=CARTESIAN_POINT('Origin',(0.144337567297406,-0.6,-0.25));
#34670=CARTESIAN_POINT('',(0.288675134594813,-0.6,0.));
#34671=CARTESIAN_POINT('',(0.144337567297406,-0.6,-0.25));
#34672=CARTESIAN_POINT('',(0.288675134594813,-0.6,0.));
#34673=CARTESIAN_POINT('',(0.144337567297406,-0.96,-0.25));
#34674=CARTESIAN_POINT('',(0.144337567297406,-0.6,-0.25));
#34675=CARTESIAN_POINT('',(0.288675134594813,-0.96,0.));
#34676=CARTESIAN_POINT('',(0.288675134594813,-0.96,0.));
#34677=CARTESIAN_POINT('',(0.288675134594813,-0.6,0.));
#34678=CARTESIAN_POINT('Origin',(-0.144337567297406,-0.6,-0.25));
#34679=CARTESIAN_POINT('',(-0.144337567297406,-0.6,-0.25));
#34680=CARTESIAN_POINT('',(0.144337567297406,-0.6,-0.25));
#34681=CARTESIAN_POINT('',(-0.144337567297406,-0.96,-0.25));
#34682=CARTESIAN_POINT('',(-0.144337567297406,-0.6,-0.25));
#34683=CARTESIAN_POINT('',(0.144337567297406,-0.96,-0.25));
#34684=CARTESIAN_POINT('Origin',(-0.288675134594813,-0.6,-8.32667268468867E-17));
#34685=CARTESIAN_POINT('',(-0.288675134594813,-0.6,-3.53525079574969E-17));
#34686=CARTESIAN_POINT('',(-0.144337567297406,-0.6,-0.25));
#34687=CARTESIAN_POINT('',(-0.288675134594813,-0.96,-5.55111512312578E-17));
#34688=CARTESIAN_POINT('',(-0.288675134594813,-0.6,-3.53525079574969E-17));
#34689=CARTESIAN_POINT('',(-0.144337567297406,-0.96,-0.25));
#34690=CARTESIAN_POINT('Origin',(-0.144337567297407,-0.6,0.25));
#34691=CARTESIAN_POINT('',(-0.144337567297407,-0.6,0.25));
#34692=CARTESIAN_POINT('',(-0.288675134594813,-0.6,-3.53525079574969E-17));
#34693=CARTESIAN_POINT('',(-0.144337567297407,-0.96,0.25));
#34694=CARTESIAN_POINT('',(-0.144337567297407,-0.6,0.25));
#34695=CARTESIAN_POINT('',(-0.288675134594813,-0.96,-3.53525079574969E-17));
#34696=CARTESIAN_POINT('Origin',(0.144337567297406,-0.6,0.25));
#34697=CARTESIAN_POINT('',(0.144337567297406,-0.6,0.25));
#34698=CARTESIAN_POINT('',(-0.144337567297407,-0.6,0.25));
#34699=CARTESIAN_POINT('',(0.144337567297406,-0.96,0.25));
#34700=CARTESIAN_POINT('',(0.144337567297406,-0.6,0.25));
#34701=CARTESIAN_POINT('',(-0.144337567297407,-0.96,0.25));
#34702=CARTESIAN_POINT('Origin',(0.288675134594813,-0.6,0.));
#34703=CARTESIAN_POINT('',(0.144337567297406,-0.6,0.25));
#34704=CARTESIAN_POINT('',(0.144337567297406,-0.96,0.25));
#34705=CARTESIAN_POINT('Origin',(0.,-0.6,0.));
#34706=CARTESIAN_POINT('Origin',(0.,-0.96,0.));
#34794=UNCERTAINTY_MEASURE_WITH_UNIT(LENGTH_MEASURE(0.001),#34852,
'DISTANCE_ACCURACY_VALUE',
'Maximum model space distance between geometric entities at asserted c
onnectivities');
#34797=UNCERTAINTY_MEASURE_WITH_UNIT(LENGTH_MEASURE(0.001),#34852,
'DISTANCE_ACCURACY_VALUE',
'Maximum model space distance between geometric entities at asserted c
onnectivities');
#34848=(
GEOMETRIC_REPRESENTATION_CONTEXT(3)
GLOBAL_UNCERTAINTY_ASSIGNED_CONTEXT((#34794))
GLOBAL_UNIT_ASSIGNED_CONTEXT((#34852,#34854,#34855))
REPRESENTATION_CONTEXT('','3D')
);
#34851=(
GEOMETRIC_REPRESENTATION_CONTEXT(3)
GLOBAL_UNCERTAINTY_ASSIGNED_CONTEXT((#34797))
GLOBAL_UNIT_ASSIGNED_CONTEXT((#34852,#34854,#34855))
REPRESENTATION_CONTEXT('','3D')
);
#34852=(
LENGTH_UNIT()
NAMED_UNIT(*)
SI_UNIT(.CENTI.,.METRE.)
);
#34854=(
NAMED_UNIT(*)
PLANE_ANGLE_UNIT()
SI_UNIT($,.RADIAN.)
);
#34855=(
NAMED_UNIT(*)
SI_UNIT($,.STERADIAN.)
SOLID_ANGLE_UNIT()
);
#34906=SHAPE_DEFINITION_REPRESENTATION(#35049,#35123);
#35049=PRODUCT_DEFINITION_SHAPE('',$,#35177);
#35123=SHAPE_REPRESENTATION('',(#15543),#34848);
#35126=PRODUCT_DEFINITION_CONTEXT('part definition',#35287,'design');
#35177=PRODUCT_DEFINITION('Cap Screw - M6x25','Cap Screw - M6x25',#35230,
#35126);
#35230=PRODUCT_DEFINITION_FORMATION('',$,#35339);
#35287=APPLICATION_CONTEXT(
'Core Data for Automotive Mechanical Design Process');
#35288=PRODUCT_CONTEXT('part definition',#35287,'mechanical');
#35339=PRODUCT('Cap Screw - M6x25','Cap Screw - M6x25',
'Cap Screw - M6x25',(#35288));
#35412=COLOUR_RGB('Black',0.12,0.14,0.17);
#35413=FILL_AREA_STYLE_COLOUR('',#35412);
#35414=FILL_AREA_STYLE('',(#35413));
#35415=SURFACE_STYLE_FILL_AREA(#35414);
#35416=SURFACE_SIDE_STYLE('',(#35415));
#35417=SURFACE_STYLE_USAGE(.BOTH.,#35416);
#35418=PRESENTATION_STYLE_ASSIGNMENT((#35417));
ENDSEC;
END-ISO-10303-21;
